ISO-10303-21;
HEADER;
FILE_DESCRIPTION (('STEP AP214'),
    '1' );
FILE_NAME ('angular contact ball bearing_68_iso_ISO 15 ABB - 1710 - 20,SI,NC,20_68.step',
    '2026-10-27T08:02:39',
    ( '' ),
    ( '' ),
    'SwSTEP 2.0',
    'SolidWorks 2026',
    '' );
FILE_SCHEMA (( 'AUTOMOTIVE_DESIGN' ));
ENDSEC;

DATA;
#15=AXIS2_PLACEMENT_3D ( 'NONE', #471, #2401, #339 ) ;
#18=APPLICATION_CONTEXT ( 'automotive_design' ) ;
#42=EDGE_CURVE ( 'NONE', #9980, #7044, #6787, .T. ) ;
#51=CIRCLE ( 'NONE', #4842, 5.525000000000000355 ) ;
#56=DIRECTION ( 'NONE',  ( 1.000000000000000000, 0.000000000000000000, 0.000000000000000000 ) ) ;
#66=VECTOR ( 'NONE', #9457, 1000.000000000000000 ) ;
#87=EDGE_CURVE ( 'NONE', #5401, #10239, #7657, .T. ) ;
#98=ORIENTED_EDGE ( 'NONE', *, *, #8688, .T. ) ;
#128=EDGE_CURVE ( 'NONE', #10292, #8107, #5580, .T. ) ;
#130=VERTEX_POINT ( 'NONE', #2582 ) ;
#135=EDGE_CURVE ( 'NONE', #9980, #9876, #10102, .T. ) ;
#140=DIRECTION ( 'NONE',  ( 1.000000000000000000, 0.000000000000000000, 0.000000000000000000 ) ) ;
#167=AXIS2_PLACEMENT_3D ( 'NONE', #171, #5883, #6935 ) ;
#171=CARTESIAN_POINT ( 'NONE',  ( 1.500000000000001332, 0.000000000000000000, 0.000000000000000000 ) ) ;
#192=EDGE_CURVE ( 'NONE', #3603, #3952, #2381, .T. ) ;
#195=DIRECTION ( 'NONE',  ( 0.000000000000000000, 0.000000000000000000, 1.000000000000000000 ) ) ;
#209=DIRECTION ( 'NONE',  ( 0.000000000000000000, 1.224646799147353207E-16, 1.000000000000000000 ) ) ;
#212=CARTESIAN_POINT ( 'NONE',  ( 0.000000000000000000, 0.000000000000000000, 0.000000000000000000 ) ) ;
#252=DIRECTION ( 'NONE',  ( 0.000000000000000000, 0.000000000000000000, -1.000000000000000000 ) ) ;
#273=PLANE ( 'NONE',  #1206 ) ;
#286=ORIENTED_EDGE ( 'NONE', *, *, #128, .F. ) ;
#302=FACE_OUTER_BOUND ( 'NONE', #521, .T. ) ;
#328=CYLINDRICAL_SURFACE ( 'NONE', #1454, 5.525000000000000355 ) ;
#339=DIRECTION ( 'NONE',  ( 0.000000000000000000, 0.000000000000000000, -1.000000000000000000 ) ) ;
#342=DIRECTION ( 'NONE',  ( 1.000000000000000000, 0.000000000000000000, 0.000000000000000000 ) ) ;
#359=( LENGTH_UNIT ( ) NAMED_UNIT ( * ) SI_UNIT ( .MILLI., .METRE. ) );
#363=ORIENTED_EDGE ( 'NONE', *, *, #11948, .F. ) ;
#366=EDGE_CURVE ( 'NONE', #11478, #710, #6798, .T. ) ;
#373=EDGE_LOOP ( 'NONE', ( #1534, #3333 ) ) ;
#377=CIRCLE ( 'NONE', #2768, 5.750000000000000000 ) ;
#408=EDGE_CURVE ( 'NONE', #2942, #11480, #10780, .T. ) ;
#444=ORIENTED_EDGE ( 'NONE', *, *, #8688, .F. ) ;
#464=LINE ( 'NONE', #3290, #7821 ) ;
#471=CARTESIAN_POINT ( 'NONE',  ( 1.399999999999999689, 0.000000000000000000, -7.399999999999999467 ) ) ;
#489=AXIS2_PLACEMENT_3D ( 'NONE', #1633, #11075, #12117 ) ;
#500=CARTESIAN_POINT ( 'NONE',  ( 1.399999999999998579, 0.000000000000000000, 0.000000000000000000 ) ) ;
#511=FACE_OUTER_BOUND ( 'NONE', #2048, .T. ) ;
#521=EDGE_LOOP ( 'NONE', ( #7403, #789, #6236, #8961 ) ) ;
#543=( NAMED_UNIT ( * ) SI_UNIT ( $, .STERADIAN. ) SOLID_ANGLE_UNIT ( ) );
#602=AXIS2_PLACEMENT_3D ( 'NONE', #2827, #9653, #11378 ) ;
#613=AXIS2_PLACEMENT_3D ( 'NONE', #3547, #857, #2536 ) ;
#660=DIRECTION ( 'NONE',  ( 0.000000000000000000, 0.000000000000000000, -1.000000000000000000 ) ) ;
#674=ORIENTED_EDGE ( 'NONE', *, *, #7139, .T. ) ;
#695=ORIENTED_EDGE ( 'NONE', *, *, #8848, .T. ) ;
#702=VERTEX_POINT ( 'NONE', #9699 ) ;
#710=VERTEX_POINT ( 'NONE', #2878 ) ;
#718=VERTEX_POINT ( 'NONE', #9000 ) ;
#720=VERTEX_POINT ( 'NONE', #5305 ) ;
#724=DIRECTION ( 'NONE',  ( -0.000000000000000000, 0.000000000000000000, 1.000000000000000000 ) ) ;
#749=EDGE_CURVE ( 'NONE', #10239, #7044, #9805, .T. ) ;
#781=VECTOR ( 'NONE', #6291, 1000.000000000000000 ) ;
#782=ORIENTED_EDGE ( 'NONE', *, *, #12280, .F. ) ;
#789=ORIENTED_EDGE ( 'NONE', *, *, #5630, .T. ) ;
#791=ADVANCED_FACE ( 'NONE', ( #302 ), #11781, .T. ) ;
#796=AXIS2_PLACEMENT_3D ( 'NONE', #6249, #10798, #2238 ) ;
#798=DIRECTION ( 'NONE',  ( 1.000000000000000000, 0.000000000000000000, 0.000000000000000000 ) ) ;
#809=EDGE_CURVE ( 'NONE', #5401, #8263, #6062, .T. ) ;
#814=CIRCLE ( 'NONE', #11987, 0.7499999999999997780 ) ;
#847=EDGE_LOOP ( 'NONE', ( #6303, #2605, #4800, #9954 ) ) ;
#855=ORIENTED_EDGE ( 'NONE', *, *, #7367, .F. ) ;
#857=DIRECTION ( 'NONE',  ( 1.000000000000000000, 0.000000000000000000, 0.000000000000000000 ) ) ;
#865=CARTESIAN_POINT ( 'NONE',  ( 1.400000000000001910, 0.000000000000000000, 0.000000000000000000 ) ) ;
#868=ADVANCED_FACE ( 'NONE', ( #4542 ), #9206, .T. ) ;
#872=DIRECTION ( 'NONE',  ( 1.000000000000000000, 0.000000000000000000, 0.000000000000000000 ) ) ;
#875=ORIENTED_EDGE ( 'NONE', *, *, #5689, .T. ) ;
#881=EDGE_LOOP ( 'NONE', ( #8333, #12231, #5450, #6422 ) ) ;
#882=LINE ( 'NONE', #1075, #4787 ) ;
#887=EDGE_CURVE ( 'NONE', #4391, #5044, #9592, .T. ) ;
#927=DIRECTION ( 'NONE',  ( 0.000000000000000000, 0.000000000000000000, -1.000000000000000000 ) ) ;
#935=DIRECTION ( 'NONE',  ( 0.000000000000000000, 0.000000000000000000, -1.000000000000000000 ) ) ;
#943=DIRECTION ( 'NONE',  ( -1.000000000000000000, -0.000000000000000000, -0.000000000000000000 ) ) ;
#944=FACE_BOUND ( 'NONE', #8542, .T. ) ;
#949=ORIENTED_EDGE ( 'NONE', *, *, #2650, .T. ) ;
#987=AXIS2_PLACEMENT_3D ( 'NONE', #10904, #3051, #6923 ) ;
#1010=CARTESIAN_POINT ( 'NONE',  ( 0.1920286436967153787, 0.000000000000000000, 0.000000000000000000 ) ) ;
#1028=STYLED_ITEM ( 'NONE', ( #3500 ), #12103 ) ;
#1047=ADVANCED_FACE ( 'NONE', ( #3054 ), #9013, .T. ) ;
#1059=ORIENTED_EDGE ( 'NONE', *, *, #9916, .T. ) ;
#1075=CARTESIAN_POINT ( 'NONE',  ( -20.63749999999999574, 0.000000000000000000, -7.500000000000000000 ) ) ;
#1078=DIRECTION ( 'NONE',  ( 1.000000000000000000, 0.000000000000000000, 0.000000000000000000 ) ) ;
#1084=CARTESIAN_POINT ( 'NONE',  ( -1.500000000000001332, 0.000000000000000000, 0.000000000000000000 ) ) ;
#1087=DIRECTION ( 'NONE',  ( 0.000000000000000000, 0.000000000000000000, 1.000000000000000000 ) ) ;
#1141=ORIENTED_EDGE ( 'NONE', *, *, #192, .F. ) ;
#1145=CARTESIAN_POINT ( 'NONE',  ( 1.500000000000001332, 0.000000000000000000, 0.000000000000000000 ) ) ;
#1180=SURFACE_STYLE_USAGE ( .BOTH. , #10695 ) ;
#1190=EDGE_CURVE ( 'NONE', #720, #7137, #8012, .T. ) ;
#1206=AXIS2_PLACEMENT_3D ( 'NONE', #6911, #2202, #10892 ) ;
#1250=ADVANCED_FACE ( 'NONE', ( #10906 ), #12179, .T. ) ;
#1285=CARTESIAN_POINT ( 'NONE',  ( 0.000000000000000000, 0.000000000000000000, 6.250000000000000000 ) ) ;
#1355=EDGE_LOOP ( 'NONE', ( #8062, #7066, #782, #5091 ) ) ;
#1377=ORIENTED_EDGE ( 'NONE', *, *, #7727, .F. ) ;
#1382=FACE_BOUND ( 'NONE', #11416, .T. ) ;
#1391=EDGE_LOOP ( 'NONE', ( #5800, #10273, #5602, #1812 ) ) ;
#1400=DIRECTION ( 'NONE',  ( 0.000000000000000000, 0.000000000000000000, -1.000000000000000000 ) ) ;
#1404=FACE_OUTER_BOUND ( 'NONE', #11301, .T. ) ;
#1432=SHAPE_REPRESENTATION_RELATIONSHIP ( 'NONE' , 'NONE' ,  #11292, #12103 ) ;
#1435=CIRCLE ( 'NONE', #2619, 7.399999999999999467 ) ;
#1454=AXIS2_PLACEMENT_3D ( 'NONE', #2754, #3707, #2640 ) ;
#1460=VERTEX_POINT ( 'NONE', #2030 ) ;
#1471=DIRECTION ( 'NONE',  ( 1.000000000000000000, 0.000000000000000000, 0.000000000000000000 ) ) ;
#1534=ORIENTED_EDGE ( 'NONE', *, *, #4320, .F. ) ;
#1538=CARTESIAN_POINT ( 'NONE',  ( 1.500000000000001332, 8.266365894244634333E-16, 6.750000000000000000 ) ) ;
#1564=ORIENTED_EDGE ( 'NONE', *, *, #3179, .F. ) ;
#1596=ORIENTED_EDGE ( 'NONE', *, *, #809, .T. ) ;
#1597=( LENGTH_UNIT ( ) NAMED_UNIT ( * ) SI_UNIT ( .MILLI., .METRE. ) );
#1633=CARTESIAN_POINT ( 'NONE',  ( -0.1920286436967153787, 0.000000000000000000, 0.000000000000000000 ) ) ;
#1674=DIRECTION ( 'NONE',  ( -1.000000000000000000, 0.000000000000000000, -0.000000000000000000 ) ) ;
#1706=ORIENTED_EDGE ( 'NONE', *, *, #9957, .F. ) ;
#1713=DIRECTION ( 'NONE',  ( 1.000000000000000000, 0.000000000000000000, 0.000000000000000000 ) ) ;
#1720=ORIENTED_EDGE ( 'NONE', *, *, #10614, .F. ) ;
#1736=DIRECTION ( 'NONE',  ( -1.000000000000000000, -0.000000000000000000, -0.000000000000000000 ) ) ;
#1745=FACE_OUTER_BOUND ( 'NONE', #2647, .T. ) ;
#1754=DIRECTION ( 'NONE',  ( 1.000000000000000000, 0.000000000000000000, 0.000000000000000000 ) ) ;
#1759=DIRECTION ( 'NONE',  ( 0.000000000000000000, 0.000000000000000000, -1.000000000000000000 ) ) ;
#1763=DIRECTION ( 'NONE',  ( 1.000000000000000000, 0.000000000000000000, 0.000000000000000000 ) ) ;
#1773=CARTESIAN_POINT ( 'NONE',  ( 1.500000000000001332, 6.766173565289127388E-16, 5.525000000000000355 ) ) ;
#1783=EDGE_CURVE ( 'NONE', #5264, #6360, #5358, .T. ) ;
#1785=ORIENTED_EDGE ( 'NONE', *, *, #887, .T. ) ;
#1787=FACE_OUTER_BOUND ( 'NONE', #881, .T. ) ;
#1791=AXIS2_PLACEMENT_3D ( 'NONE', #10153, #1713, #4336 ) ;
#1812=ORIENTED_EDGE ( 'NONE', *, *, #2041, .T. ) ;
#1820=CYLINDRICAL_SURFACE ( 'NONE', #3843, 5.000000000000000000 ) ;
#1858=PRODUCT_DEFINITION_FORMATION_WITH_SPECIFIED_SOURCE ( 'ANY', '', #3037, .NOT_KNOWN. ) ;
#1865=ORIENTED_EDGE ( 'NONE', *, *, #8072, .T. ) ;
#1867=DIRECTION ( 'NONE',  ( 1.000000000000000000, 0.000000000000000000, 0.000000000000000000 ) ) ;
#1870=VERTEX_POINT ( 'NONE', #10261 ) ;
#1886=DIRECTION ( 'NONE',  ( 0.000000000000000000, -1.000000000000000000, 0.000000000000000000 ) ) ;
#1891=DIRECTION ( 'NONE',  ( 0.000000000000000000, 0.000000000000000000, -1.000000000000000000 ) ) ;
#1896=CARTESIAN_POINT ( 'NONE',  ( 0.1920286436967153787, 7.516269729766880368E-16, -5.525000000000000355 ) ) ;
#1942=ORIENTED_EDGE ( 'NONE', *, *, #6609, .T. ) ;
#1946=CARTESIAN_POINT ( 'NONE',  ( -1.399999999999998579, 0.000000000000000000, -7.500000000000000000 ) ) ;
#1964=EDGE_CURVE ( 'NONE', #1870, #4934, #8008, .T. ) ;
#1971=CIRCLE ( 'NONE', #11952, 0.1000000000000002554 ) ;
#1980=VECTOR ( 'NONE', #872, 1000.000000000000000 ) ;
#2025=UNCERTAINTY_MEASURE_WITH_UNIT (LENGTH_MEASURE( 1.000000000000000082E-05 ), #359, 'distance_accuracy_value', 'NONE');
#2030=CARTESIAN_POINT ( 'NONE',  ( -1.400000000000001910, 0.000000000000000000, -5.000000000000000000 ) ) ;
#2032=CARTESIAN_POINT ( 'NONE',  ( 1.400000000000000133, 6.245698675651501825E-16, 5.100000000000000533 ) ) ;
#2041=EDGE_CURVE ( 'NONE', #5044, #4391, #6818, .T. ) ;
#2047=CIRCLE ( 'NONE', #5042, 5.100000000000000533 ) ;
#2048=EDGE_LOOP ( 'NONE', ( #3542, #1377 ) ) ;
#2099=ORIENTED_EDGE ( 'NONE', *, *, #10349, .T. ) ;
#2187=AXIS2_PLACEMENT_3D ( 'NONE', #1084, #9658, #2831 ) ;
#2202=DIRECTION ( 'NONE',  ( -1.000000000000000000, 0.000000000000000000, -0.000000000000000000 ) ) ;
#2233=CIRCLE ( 'NONE', #4642, 0.1000000000000002554 ) ;
#2238=DIRECTION ( 'NONE',  ( 0.000000000000000000, 0.000000000000000000, -1.000000000000000000 ) ) ;
#2247=DIRECTION ( 'NONE',  ( 0.000000000000000000, 0.000000000000000000, -1.000000000000000000 ) ) ;
#2264=CARTESIAN_POINT ( 'NONE',  ( -20.63749999999999574, 9.184850993605147944E-16, 7.500000000000000000 ) ) ;
#2268=CARTESIAN_POINT ( 'NONE',  ( 1.500000000000001332, 0.000000000000000000, -6.750000000000000000 ) ) ;
#2278=ORIENTED_EDGE ( 'NONE', *, *, #1964, .F. ) ;
#2300=DIRECTION ( 'NONE',  ( 0.000000000000000000, 0.000000000000000000, 1.000000000000000000 ) ) ;
#2302=( NAMED_UNIT ( * ) SI_UNIT ( $, .STERADIAN. ) SOLID_ANGLE_UNIT ( ) );
#2308=CARTESIAN_POINT ( 'NONE',  ( -1.500000000000001332, 0.000000000000000000, 0.000000000000000000 ) ) ;
#2339=CARTESIAN_POINT ( 'NONE',  ( -1.400000000000000133, 0.000000000000000000, 0.000000000000000000 ) ) ;
#2344=DIRECTION ( 'NONE',  ( 1.000000000000000000, 0.000000000000000000, 0.000000000000000000 ) ) ;
#2347=ORIENTED_EDGE ( 'NONE', *, *, #87, .T. ) ;
#2351=DIRECTION ( 'NONE',  ( 1.000000000000000000, 0.000000000000000000, 0.000000000000000000 ) ) ;
#2381=CIRCLE ( 'NONE', #11757, 6.975000000000000533 ) ;
#2393=CARTESIAN_POINT ( 'NONE',  ( 0.000000000000000000, 0.000000000000000000, 6.250000000000000000 ) ) ;
#2401=DIRECTION ( 'NONE',  ( 0.000000000000000000, -1.000000000000000000, 0.000000000000000000 ) ) ;
#2404=CYLINDRICAL_SURFACE ( 'NONE', #8421, 6.975000000000000533 ) ;
#2406=ORIENTED_EDGE ( 'NONE', *, *, #42, .T. ) ;
#2415=DIRECTION ( 'NONE',  ( 0.000000000000000000, 0.000000000000000000, -1.000000000000000000 ) ) ;
#2467=AXIS2_PLACEMENT_3D ( 'NONE', #11623, #10807, #3079 ) ;
#2472=DIRECTION ( 'NONE',  ( 0.000000000000000000, 0.000000000000000000, -1.000000000000000000 ) ) ;
#2476=EDGE_LOOP ( 'NONE', ( #2787, #1706, #9471, #3437 ) ) ;
#2484=ORIENTED_EDGE ( 'NONE', *, *, #42, .F. ) ;
#2492=ADVANCED_FACE ( 'NONE', ( #1404 ), #2404, .F. ) ;
#2514=DIRECTION ( 'NONE',  ( 0.000000000000000000, 0.000000000000000000, -1.000000000000000000 ) ) ;
#2536=DIRECTION ( 'NONE',  ( 0.000000000000000000, 0.000000000000000000, -1.000000000000000000 ) ) ;
#2580=TOROIDAL_SURFACE ( 'NONE', #9389, 7.399999999999999467, 0.1000000000000000472 ) ;
#2582=CARTESIAN_POINT ( 'NONE',  ( -1.500000000000001332, 8.541911424052788811E-16, 6.975000000000000533 ) ) ;
#2590=DIRECTION ( 'NONE',  ( 0.000000000000000000, 0.000000000000000000, -1.000000000000000000 ) ) ;
#2597=PLANE ( 'NONE',  #4213 ) ;
#2598=FACE_OUTER_BOUND ( 'NONE', #8133, .T. ) ;
#2605=ORIENTED_EDGE ( 'NONE', *, *, #5155, .T. ) ;
#2609=CIRCLE ( 'NONE', #11798, 0.7499999999999997780 ) ;
#2615=MECHANICAL_DESIGN_GEOMETRIC_PRESENTATION_REPRESENTATION('',(#1028),#9040);
#2619=AXIS2_PLACEMENT_3D ( 'NONE', #1145, #2858, #6491 ) ;
#2638=CARTESIAN_POINT ( 'NONE',  ( -1.399999999999998579, 0.000000000000000000, 0.000000000000000000 ) ) ;
#2640=DIRECTION ( 'NONE',  ( 0.000000000000000000, 0.000000000000000000, -1.000000000000000000 ) ) ;
#2646=CARTESIAN_POINT ( 'NONE',  ( 0.000000000000000000, 7.654042494670957606E-16, -6.250000000000000000 ) ) ;
#2647=EDGE_LOOP ( 'NONE', ( #9997, #9816, #1059, #12141 ) ) ;
#2650=EDGE_CURVE ( 'NONE', #130, #3603, #7353, .T. ) ;
#2668=CIRCLE ( 'NONE', #2467, 5.100000000000000533 ) ;
#2673=ORIENTED_EDGE ( 'NONE', *, *, #6635, .F. ) ;
#2677=DIRECTION ( 'NONE',  ( 0.000000000000000000, 0.000000000000000000, 1.000000000000000000 ) ) ;
#2701=CARTESIAN_POINT ( 'NONE',  ( -20.63749999999999574, 0.000000000000000000, 0.000000000000000000 ) ) ;
#2703=ADVANCED_FACE ( 'NONE', ( #8482 ), #4592, .T. ) ;
#2712=EDGE_CURVE ( 'NONE', #1460, #5665, #5224, .T. ) ;
#2714=CARTESIAN_POINT ( 'NONE',  ( -1.400000000000001910, 0.000000000000000000, 0.000000000000000000 ) ) ;
#2741=CARTESIAN_POINT ( 'NONE',  ( -20.63749999999999574, 0.000000000000000000, 0.000000000000000000 ) ) ;
#2747=DIRECTION ( 'NONE',  ( 0.000000000000000000, 0.000000000000000000, -1.000000000000000000 ) ) ;
#2754=CARTESIAN_POINT ( 'NONE',  ( -20.63749999999999929, 0.000000000000000000, 0.000000000000000000 ) ) ;
#2763=AXIS2_PLACEMENT_3D ( 'NONE', #2741, #3883, #11490 ) ;
#2768=AXIS2_PLACEMENT_3D ( 'NONE', #10060, #9070, #2415 ) ;
#2775=ORIENTED_EDGE ( 'NONE', *, *, #4149, .T. ) ;
#2787=ORIENTED_EDGE ( 'NONE', *, *, #809, .F. ) ;
#2793=CIRCLE ( 'NONE', #6393, 7.500000000000000000 ) ;
#2805=CYLINDRICAL_SURFACE ( 'NONE', #2763, 6.750000000000000000 ) ;
#2807=AXIS2_PLACEMENT_3D ( 'NONE', #6714, #1078, #10568 ) ;
#2827=CARTESIAN_POINT ( 'NONE',  ( -1.500000000000001332, 0.000000000000000000, 0.000000000000000000 ) ) ;
#2828=DIRECTION ( 'NONE',  ( 1.000000000000000000, 0.000000000000000000, 0.000000000000000000 ) ) ;
#2831=DIRECTION ( 'NONE',  ( 0.000000000000000000, 0.000000000000000000, -1.000000000000000000 ) ) ;
#2846=AXIS2_PLACEMENT_3D ( 'NONE', #10387, #4650, #12311 ) ;
#2858=DIRECTION ( 'NONE',  ( 1.000000000000000000, 0.000000000000000000, 0.000000000000000000 ) ) ;
#2864=DIRECTION ( 'NONE',  ( -1.000000000000000000, -0.000000000000000000, -0.000000000000000000 ) ) ;
#2874=EDGE_LOOP ( 'NONE', ( #11142, #7666, #363, #7895 ) ) ;
#2875=CARTESIAN_POINT ( 'NONE',  ( 1.500000000000000888, 6.245698675651501825E-16, 5.100000000000000533 ) ) ;
#2878=CARTESIAN_POINT ( 'NONE',  ( 1.500000000000001332, 9.123618653647779187E-16, 7.399999999999999467 ) ) ;
#2880=CARTESIAN_POINT ( 'NONE',  ( -20.63749999999999574, 0.000000000000000000, -6.975000000000000533 ) ) ;
#2882=ORIENTED_EDGE ( 'NONE', *, *, #4483, .T. ) ;
#2942=VERTEX_POINT ( 'NONE', #8968 ) ;
#2975=EDGE_LOOP ( 'NONE', ( #10371, #11187, #11090, #98 ) ) ;
#3037=PRODUCT ( 'angular contact ball bearing_68_iso_ISO 15 ABB - 1710 - 20,SI,NC,20_68', 'angular contact ball bearing_68_iso_ISO 15 ABB - 1710 - 20,SI,NC,20_68', '', ( #12216 ) ) ;
#3039=AXIS2_PLACEMENT_3D ( 'NONE', #8416, #3665, #2472 ) ;
#3049=CIRCLE ( 'NONE', #4426, 5.525000000000000355 ) ;
#3051=DIRECTION ( 'NONE',  ( -0.000000000000000000, 1.000000000000000000, 1.224646799147353207E-16 ) ) ;
#3054=FACE_OUTER_BOUND ( 'NONE', #847, .T. ) ;
#3066=AXIS2_PLACEMENT_3D ( 'NONE', #9453, #8450, #10369 ) ;
#3073=APPLICATION_CONTEXT ( 'automotive_design' ) ;
#3079=DIRECTION ( 'NONE',  ( 0.000000000000000000, 0.000000000000000000, -1.000000000000000000 ) ) ;
#3080=FILL_AREA_STYLE ('',( #11624 ) ) ;
#3125=ORIENTED_EDGE ( 'NONE', *, *, #8029, .T. ) ;
#3162=ORIENTED_EDGE ( 'NONE', *, *, #5155, .F. ) ;
#3179=EDGE_CURVE ( 'NONE', #11480, #2942, #2047, .T. ) ;
#3198=DIRECTION ( 'NONE',  ( 0.000000000000000000, 1.224646799147343593E-16, 1.000000000000000000 ) ) ;
#3209=ADVANCED_FACE ( 'NONE', ( #7468 ), #11264, .T. ) ;
#3252=CIRCLE ( 'NONE', #11021, 0.1000000000000002554 ) ;
#3268=CARTESIAN_POINT ( 'NONE',  ( -20.63749999999999929, 0.000000000000000000, -5.750000000000000000 ) ) ;
#3271=ADVANCED_FACE ( 'NONE', ( #11559, #944 ), #6580, .T. ) ;
#3279=CARTESIAN_POINT ( 'NONE',  ( 1.399999999999998579, 9.184850993605147944E-16, 7.500000000000000000 ) ) ;
#3290=CARTESIAN_POINT ( 'NONE',  ( -20.63749999999999574, 8.266365894244634333E-16, 6.750000000000000000 ) ) ;
#3333=ORIENTED_EDGE ( 'NONE', *, *, #11274, .F. ) ;
#3343=LINE ( 'NONE', #10039, #5212 ) ;
#3347=CARTESIAN_POINT ( 'NONE',  ( -0.5590169943749470072, 7.041719095097280880E-16, 5.750000000000000000 ) ) ;
#3414=DIRECTION ( 'NONE',  ( 0.000000000000000000, 0.000000000000000000, -1.000000000000000000 ) ) ;
#3437=ORIENTED_EDGE ( 'NONE', *, *, #11603, .F. ) ;
#3443=CARTESIAN_POINT ( 'NONE',  ( 1.399999999999999689, 9.062386313690412402E-16, 7.399999999999999467 ) ) ;
#3500=PRESENTATION_STYLE_ASSIGNMENT (( #1180 ) ) ;
#3531=CARTESIAN_POINT ( 'NONE',  ( -20.63749999999999929, 0.000000000000000000, -5.525000000000000355 ) ) ;
#3542=ORIENTED_EDGE ( 'NONE', *, *, #5949, .F. ) ;
#3547=CARTESIAN_POINT ( 'NONE',  ( 1.500000000000001332, 0.000000000000000000, 0.000000000000000000 ) ) ;
#3582=DIRECTION ( 'NONE',  ( 1.000000000000000000, 0.000000000000000000, 0.000000000000000000 ) ) ;
#3590=CIRCLE ( 'NONE', #2187, 7.399999999999999467 ) ;
#3603=VERTEX_POINT ( 'NONE', #9326 ) ;
#3607=DIRECTION ( 'NONE',  ( 0.000000000000000000, 0.000000000000000000, -1.000000000000000000 ) ) ;
#3627=AXIS2_PLACEMENT_3D ( 'NONE', #2714, #7482, #660 ) ;
#3633=LINE ( 'NONE', #10311, #66 ) ;
#3665=DIRECTION ( 'NONE',  ( 1.000000000000000000, 0.000000000000000000, 0.000000000000000000 ) ) ;
#3676=ADVANCED_FACE ( 'NONE', ( #9566 ), #4453, .T. ) ;
#3707=DIRECTION ( 'NONE',  ( 1.000000000000000000, 0.000000000000000000, 0.000000000000000000 ) ) ;
#3709=ORIENTED_EDGE ( 'NONE', *, *, #8848, .F. ) ;
#3727=CARTESIAN_POINT ( 'NONE',  ( -1.500000000000001332, 0.000000000000000000, 0.000000000000000000 ) ) ;
#3736=FACE_OUTER_BOUND ( 'NONE', #4859, .T. ) ;
#3740=ADVANCED_FACE ( 'NONE', ( #5692 ), #3815, .F. ) ;
#3768=TOROIDAL_SURFACE ( 'NONE', #7166, 6.250000000000000000, 0.7500000000000000000 ) ;
#3806=CARTESIAN_POINT ( 'NONE',  ( -1.400000000000001910, 6.123233995736766282E-16, 5.000000000000000000 ) ) ;
#3812=AXIS2_PLACEMENT_3D ( 'NONE', #9363, #10237, #12096 ) ;
#3815=CYLINDRICAL_SURFACE ( 'NONE', #8860, 6.750000000000000000 ) ;
#3825=CARTESIAN_POINT ( 'NONE',  ( 1.399999999999999689, 0.000000000000000000, 0.000000000000000000 ) ) ;
#3843=AXIS2_PLACEMENT_3D ( 'NONE', #10452, #5752, #1891 ) ;
#3856=EDGE_LOOP ( 'NONE', ( #674, #10337 ) ) ;
#3881=MECHANICAL_DESIGN_GEOMETRIC_PRESENTATION_REPRESENTATION('',(#9073),#11055);
#3883=DIRECTION ( 'NONE',  ( 1.000000000000000000, 0.000000000000000000, 0.000000000000000000 ) ) ;
#3901=DIRECTION ( 'NONE',  ( 0.000000000000000000, 0.000000000000000000, -1.000000000000000000 ) ) ;
#3913=ORIENTED_EDGE ( 'NONE', *, *, #4888, .T. ) ;
#3928=EDGE_LOOP ( 'NONE', ( #2484, #10016, #2347, #12257 ) ) ;
#3952=VERTEX_POINT ( 'NONE', #4065 ) ;
#4029=DIRECTION ( 'NONE',  ( 0.000000000000000000, 1.000000000000000000, -1.224646799147353207E-16 ) ) ;
#4035=DIRECTION ( 'NONE',  ( 0.000000000000000000, 0.000000000000000000, 1.000000000000000000 ) ) ;
#4065=CARTESIAN_POINT ( 'NONE',  ( -0.1920286436967154065, 8.541911424052788811E-16, -6.975000000000000533 ) ) ;
#4067=CARTESIAN_POINT ( 'NONE',  ( -1.400000000000000133, 0.000000000000000000, -5.100000000000000533 ) ) ;
#4110=EDGE_CURVE ( 'NONE', #718, #5264, #5657, .T. ) ;
#4119=VERTEX_POINT ( 'NONE', #7643 ) ;
#4142=DIRECTION ( 'NONE',  ( 1.000000000000000000, 0.000000000000000000, 0.000000000000000000 ) ) ;
#4149=EDGE_CURVE ( 'NONE', #5665, #702, #3633, .T. ) ;
#4157=ORIENTED_EDGE ( 'NONE', *, *, #4302, .T. ) ;
#4186=DIRECTION ( 'NONE',  ( 1.000000000000000000, 0.000000000000000000, 0.000000000000000000 ) ) ;
#4208=CIRCLE ( 'NONE', #7029, 5.100000000000000533 ) ;
#4213=AXIS2_PLACEMENT_3D ( 'NONE', #8428, #1674, #724 ) ;
#4235=DIRECTION ( 'NONE',  ( 1.000000000000000000, 0.000000000000000000, 0.000000000000000000 ) ) ;
#4257=ORIENTED_EDGE ( 'NONE', *, *, #408, .T. ) ;
#4302=EDGE_CURVE ( 'NONE', #1460, #2942, #5068, .T. ) ;
#4317=CARTESIAN_POINT ( 'NONE',  ( -1.400000000000001910, 0.000000000000000000, 0.000000000000000000 ) ) ;
#4320=EDGE_CURVE ( 'NONE', #5423, #5710, #2668, .T. ) ;
#4336=DIRECTION ( 'NONE',  ( 0.000000000000000000, 0.000000000000000000, -1.000000000000000000 ) ) ;
#4350=DIRECTION ( 'NONE',  ( 0.000000000000000000, 0.000000000000000000, 1.000000000000000000 ) ) ;
#4380=MANIFOLD_SOLID_BREP ( 'OuterRace', #5389 ) ;
#4387=EDGE_LOOP ( 'NONE', ( #11220, #2406, #3913, #8689 ) ) ;
#4391=VERTEX_POINT ( 'NONE', #1538 ) ;
#4411=( NAMED_UNIT ( * ) PLANE_ANGLE_UNIT ( ) SI_UNIT ( $, .RADIAN. ) );
#4426=AXIS2_PLACEMENT_3D ( 'NONE', #6595, #9411, #11094 ) ;
#4453=TOROIDAL_SURFACE ( 'NONE', #3066, 6.250000000000000000, 0.7500000000000000000 ) ;
#4483=EDGE_CURVE ( 'NONE', #7385, #130, #9477, .T. ) ;
#4501=CIRCLE ( 'NONE', #11086, 0.1000000000000002554 ) ;
#4504=ORIENTED_EDGE ( 'NONE', *, *, #11106, .T. ) ;
#4508=DIRECTION ( 'NONE',  ( 1.000000000000000000, 0.000000000000000000, 0.000000000000000000 ) ) ;
#4542=FACE_OUTER_BOUND ( 'NONE', #7228, .T. ) ;
#4570=AXIS2_PLACEMENT_3D ( 'NONE', #6264, #10078, #5320 ) ;
#4581=DIRECTION ( 'NONE',  ( 0.000000000000000000, 0.000000000000000000, -1.000000000000000000 ) ) ;
#4592=CYLINDRICAL_SURFACE ( 'NONE', #3039, 5.750000000000000000 ) ;
#4613=CYLINDRICAL_SURFACE ( 'NONE', #9970, 5.750000000000000000 ) ;
#4640=CARTESIAN_POINT ( 'NONE',  ( -1.400000000000000133, 6.245698675651501825E-16, 5.100000000000000533 ) ) ;
#4642=AXIS2_PLACEMENT_3D ( 'NONE', #2032, #4029, #209 ) ;
#4650=DIRECTION ( 'NONE',  ( 1.000000000000000000, 0.000000000000000000, 0.000000000000000000 ) ) ;
#4708=EDGE_LOOP ( 'NONE', ( #10926, #949, #3162, #9172 ) ) ;
#4742=ORIENTED_EDGE ( 'NONE', *, *, #887, .F. ) ;
#4763=CARTESIAN_POINT ( 'NONE',  ( 1.500000000000001332, 0.000000000000000000, 0.000000000000000000 ) ) ;
#4787=VECTOR ( 'NONE', #4887, 1000.000000000000000 ) ;
#4793=DIRECTION ( 'NONE',  ( 0.000000000000000000, 0.000000000000000000, 1.000000000000000000 ) ) ;
#4800=ORIENTED_EDGE ( 'NONE', *, *, #11048, .T. ) ;
#4815=VECTOR ( 'NONE', #12084, 1000.000000000000000 ) ;
#4820=FACE_OUTER_BOUND ( 'NONE', #2975, .T. ) ;
#4842=AXIS2_PLACEMENT_3D ( 'NONE', #1010, #943, #195 ) ;
#4843=AXIS2_PLACEMENT_3D ( 'NONE', #11042, #2344, #3414 ) ;
#4859=EDGE_LOOP ( 'NONE', ( #2673, #8874, #4157, #1564 ) ) ;
#4887=DIRECTION ( 'NONE',  ( 1.000000000000000000, 0.000000000000000000, 0.000000000000000000 ) ) ;
#4888=EDGE_CURVE ( 'NONE', #7044, #10239, #10259, .T. ) ;
#4916=CARTESIAN_POINT ( 'NONE',  ( -1.500000000000001332, 0.000000000000000000, 0.000000000000000000 ) ) ;
#4934=VERTEX_POINT ( 'NONE', #7589 ) ;
#4964=ORIENTED_EDGE ( 'NONE', *, *, #4483, .F. ) ;
#4973=DIRECTION ( 'NONE',  ( 1.000000000000000000, 0.000000000000000000, 0.000000000000000000 ) ) ;
#4986=AXIS2_PLACEMENT_3D ( 'NONE', #4916, #4973, #6871 ) ;
#5036=ORIENTED_EDGE ( 'NONE', *, *, #2712, .T. ) ;
#5042=AXIS2_PLACEMENT_3D ( 'NONE', #6283, #3582, #7401 ) ;
#5044=VERTEX_POINT ( 'NONE', #2268 ) ;
#5056=EDGE_LOOP ( 'NONE', ( #11298, #3125, #1942, #7788 ) ) ;
#5068=CIRCLE ( 'NONE', #6464, 0.1000000000000002554 ) ;
#5071=DIRECTION ( 'NONE',  ( 0.000000000000000000, 1.000000000000000000, -1.224646799147353207E-16 ) ) ;
#5086=AXIS2_PLACEMENT_3D ( 'NONE', #12317, #5765, #1087 ) ;
#5089=FACE_OUTER_BOUND ( 'NONE', #2476, .T. ) ;
#5091=ORIENTED_EDGE ( 'NONE', *, *, #1190, .F. ) ;
#5145=ORIENTED_EDGE ( 'NONE', *, *, #2041, .F. ) ;
#5155=EDGE_CURVE ( 'NONE', #3952, #3603, #9298, .T. ) ;
#5174=AXIS2_PLACEMENT_3D ( 'NONE', #1285, #8923, #1400 ) ;
#5175=CARTESIAN_POINT ( 'NONE',  ( 0.000000000000000000, 0.000000000000000000, 0.000000000000000000 ) ) ;
#5212=VECTOR ( 'NONE', #1471, 1000.000000000000000 ) ;
#5224=CIRCLE ( 'NONE', #3627, 5.000000000000000000 ) ;
#5241=ADVANCED_FACE ( 'NONE', ( #9460 ), #9646, .F. ) ;
#5264=VERTEX_POINT ( 'NONE', #1946 ) ;
#5276=AXIS2_PLACEMENT_3D ( 'NONE', #3727, #5668, #8543 ) ;
#5278=DIRECTION ( 'NONE',  ( 0.000000000000000000, 0.000000000000000000, -1.000000000000000000 ) ) ;
#5304=ORIENTED_EDGE ( 'NONE', *, *, #11251, .T. ) ;
#5305=CARTESIAN_POINT ( 'NONE',  ( 1.399999999999998579, 0.000000000000000000, -7.500000000000000000 ) ) ;
#5320=DIRECTION ( 'NONE',  ( 0.000000000000000000, 0.000000000000000000, -1.000000000000000000 ) ) ;
#5329=EDGE_LOOP ( 'NONE', ( #8779, #6362, #695, #855 ) ) ;
#5340=EDGE_LOOP ( 'NONE', ( #6681, #1596, #9723, #8183 ) ) ;
#5358=CIRCLE ( 'NONE', #12330, 7.500000000000000000 ) ;
#5366=( NAMED_UNIT ( * ) PLANE_ANGLE_UNIT ( ) SI_UNIT ( $, .RADIAN. ) );
#5389=CLOSED_SHELL ( 'NONE', ( #6558, #12045, #791, #11256, #10448, #10562, #1250, #5241, #7307, #2703, #9976, #10751, #3676, #9784, #10912, #9682, #10342, #6532, #8996, #6116, #1047, #3740, #2492, #6135, #3209, #868, #3271, #6245 ) ) ;
#5392=CIRCLE ( 'NONE', #4986, 6.975000000000000533 ) ;
#5401=VERTEX_POINT ( 'NONE', #11686 ) ;
#5414=VECTOR ( 'NONE', #7012, 1000.000000000000000 ) ;
#5423=VERTEX_POINT ( 'NONE', #10697 ) ;
#5427=TOROIDAL_SURFACE ( 'NONE', #7833, 5.100000000000000533, 0.1000000000000001582 ) ;
#5428=AXIS2_PLACEMENT_3D ( 'NONE', #10147, #1763, #4581 ) ;
#5429=VERTEX_POINT ( 'NONE', #5946 ) ;
#5450=ORIENTED_EDGE ( 'NONE', *, *, #4110, .T. ) ;
#5468=EDGE_CURVE ( 'NONE', #4934, #1870, #9891, .T. ) ;
#5501=DIRECTION ( 'NONE',  ( 0.000000000000000000, 1.224646799147343593E-16, 1.000000000000000000 ) ) ;
#5532=CARTESIAN_POINT ( 'NONE',  ( -20.63749999999999574, 8.541911424052788811E-16, 6.975000000000000533 ) ) ;
#5580=CIRCLE ( 'NONE', #1791, 5.750000000000000000 ) ;
#5602=ORIENTED_EDGE ( 'NONE', *, *, #10614, .T. ) ;
#5606=DIRECTION ( 'NONE',  ( 0.000000000000000000, 0.000000000000000000, -1.000000000000000000 ) ) ;
#5630=EDGE_CURVE ( 'NONE', #4119, #6360, #4501, .T. ) ;
#5657=CIRCLE ( 'NONE', #11442, 0.1000000000000002554 ) ;
#5665=VERTEX_POINT ( 'NONE', #3806 ) ;
#5668=DIRECTION ( 'NONE',  ( 1.000000000000000000, 0.000000000000000000, 0.000000000000000000 ) ) ;
#5686=CARTESIAN_POINT ( 'NONE',  ( 0.5590169943749478954, 8.266365894244635319E-16, -6.750000000000000000 ) ) ;
#5689=EDGE_CURVE ( 'NONE', #702, #5429, #10490, .T. ) ;
#5692=FACE_OUTER_BOUND ( 'NONE', #1391, .T. ) ;
#5710=VERTEX_POINT ( 'NONE', #2875 ) ;
#5722=EDGE_LOOP ( 'NONE', ( #2278, #11622 ) ) ;
#5736=DIRECTION ( 'NONE',  ( 1.000000000000000000, 0.000000000000000000, 0.000000000000000000 ) ) ;
#5752=DIRECTION ( 'NONE',  ( 1.000000000000000000, 0.000000000000000000, 0.000000000000000000 ) ) ;
#5765=DIRECTION ( 'NONE',  ( 1.000000000000000000, 0.000000000000000000, 0.000000000000000000 ) ) ;
#5800=ORIENTED_EDGE ( 'NONE', *, *, #11050, .F. ) ;
#5823=AXIS2_PLACEMENT_3D ( 'NONE', #12336, #6608, #3607 ) ;
#5868=CARTESIAN_POINT ( 'NONE',  ( -1.399999999999998579, 0.000000000000000000, 0.000000000000000000 ) ) ;
#5883=DIRECTION ( 'NONE',  ( 1.000000000000000000, 0.000000000000000000, 0.000000000000000000 ) ) ;
#5940=DIRECTION ( 'NONE',  ( -1.000000000000000000, -0.000000000000000000, -0.000000000000000000 ) ) ;
#5942=ORIENTED_EDGE ( 'NONE', *, *, #749, .F. ) ;
#5946=CARTESIAN_POINT ( 'NONE',  ( 1.400000000000001910, 0.000000000000000000, -5.000000000000000000 ) ) ;
#5949=EDGE_CURVE ( 'NONE', #718, #4119, #8227, .T. ) ;
#5981=DIRECTION ( 'NONE',  ( 0.000000000000000000, 0.000000000000000000, -1.000000000000000000 ) ) ;
#6044=AXIS2_PLACEMENT_3D ( 'NONE', #6183, #8946, #2247 ) ;
#6056=AXIS2_PLACEMENT_3D ( 'NONE', #212, #4035, #8864 ) ;
#6062=LINE ( 'NONE', #7996, #7806 ) ;
#6116=ADVANCED_FACE ( 'NONE', ( #12148, #8548 ), #2597, .T. ) ;
#6128=DIRECTION ( 'NONE',  ( 1.000000000000000000, 0.000000000000000000, 0.000000000000000000 ) ) ;
#6135=ADVANCED_FACE ( 'NONE', ( #1787 ), #11196, .T. ) ;
#6140=PRODUCT_DEFINITION_CONTEXT ( 'detailed design', #3073, 'design' ) ;
#6166=EDGE_CURVE ( 'NONE', #710, #7137, #1435, .T. ) ;
#6183=CARTESIAN_POINT ( 'NONE',  ( 1.399999999999998579, 0.000000000000000000, 0.000000000000000000 ) ) ;
#6236=ORIENTED_EDGE ( 'NONE', *, *, #1783, .F. ) ;
#6243=AXIS2_PLACEMENT_3D ( 'NONE', #2701, #10321, #2514 ) ;
#6245=ADVANCED_FACE ( 'NONE', ( #1382, #511 ), #273, .T. ) ;
#6249=CARTESIAN_POINT ( 'NONE',  ( -1.399999999999999689, 0.000000000000000000, 0.000000000000000000 ) ) ;
#6264=CARTESIAN_POINT ( 'NONE',  ( 1.400000000000000133, 0.000000000000000000, 0.000000000000000000 ) ) ;
#6272=ORIENTED_EDGE ( 'NONE', *, *, #6166, .F. ) ;
#6283=CARTESIAN_POINT ( 'NONE',  ( -1.500000000000001332, 0.000000000000000000, 0.000000000000000000 ) ) ;
#6291=DIRECTION ( 'NONE',  ( 1.000000000000000000, 0.000000000000000000, 0.000000000000000000 ) ) ;
#6303=ORIENTED_EDGE ( 'NONE', *, *, #11251, .F. ) ;
#6312=ORIENTED_EDGE ( 'NONE', *, *, #6635, .T. ) ;
#6320=CARTESIAN_POINT ( 'NONE',  ( -20.63749999999999929, 0.000000000000000000, -5.000000000000000000 ) ) ;
#6360=VERTEX_POINT ( 'NONE', #7209 ) ;
#6362=ORIENTED_EDGE ( 'NONE', *, *, #5468, .T. ) ;
#6393=AXIS2_PLACEMENT_3D ( 'NONE', #5868, #10726, #12342 ) ;
#6422=ORIENTED_EDGE ( 'NONE', *, *, #8029, .F. ) ;
#6426=( GEOMETRIC_REPRESENTATION_CONTEXT ( 3 ) GLOBAL_UNCERTAINTY_ASSIGNED_CONTEXT ( ( #2025 ) ) GLOBAL_UNIT_ASSIGNED_CONTEXT ( ( #359, #10873, #2302 ) ) REPRESENTATION_CONTEXT ( 'NONE', 'WORKASPACE' ) );
#6435=CARTESIAN_POINT ( 'NONE',  ( 0.000000000000000000, 0.000000000000000000, 0.000000000000000000 ) ) ;
#6440=CARTESIAN_POINT ( 'NONE',  ( -1.399999999999999689, 9.062386313690412402E-16, 7.399999999999999467 ) ) ;
#6451=EDGE_LOOP ( 'NONE', ( #8309, #2775, #875, #11386 ) ) ;
#6464=AXIS2_PLACEMENT_3D ( 'NONE', #4067, #9756, #8002 ) ;
#6476=EDGE_CURVE ( 'NONE', #5665, #1460, #11971, .T. ) ;
#6491=DIRECTION ( 'NONE',  ( 0.000000000000000000, 0.000000000000000000, -1.000000000000000000 ) ) ;
#6520=ORIENTED_EDGE ( 'NONE', *, *, #6166, .T. ) ;
#6521=CARTESIAN_POINT ( 'NONE',  ( 1.400000000000000133, 0.000000000000000000, -5.100000000000000533 ) ) ;
#6532=ADVANCED_FACE ( 'NONE', ( #4820 ), #1820, .F. ) ;
#6558=ADVANCED_FACE ( 'NONE', ( #7713 ), #2580, .T. ) ;
#6560=TOROIDAL_SURFACE ( 'NONE', #9775, 5.100000000000000533, 0.1000000000000001582 ) ;
#6580=PLANE ( 'NONE',  #2846 ) ;
#6592=AXIS2_PLACEMENT_3D ( 'NONE', #2308, #6128, #7010 ) ;
#6595=CARTESIAN_POINT ( 'NONE',  ( 0.1920286436967153787, 0.000000000000000000, 0.000000000000000000 ) ) ;
#6608=DIRECTION ( 'NONE',  ( 1.000000000000000000, 0.000000000000000000, 0.000000000000000000 ) ) ;
#6609=EDGE_CURVE ( 'NONE', #5264, #720, #882, .T. ) ;
#6635=EDGE_CURVE ( 'NONE', #5665, #11480, #1971, .T. ) ;
#6641=AXIS2_PLACEMENT_3D ( 'NONE', #4317, #1754, #7393 ) ;
#6681=ORIENTED_EDGE ( 'NONE', *, *, #9355, .F. ) ;
#6714=CARTESIAN_POINT ( 'NONE',  ( 1.400000000000001910, 0.000000000000000000, 0.000000000000000000 ) ) ;
#6770=ORIENTED_EDGE ( 'NONE', *, *, #10152, .T. ) ;
#6787=CIRCLE ( 'NONE', #987, 0.7499999999999997780 ) ;
#6798=CIRCLE ( 'NONE', #7394, 0.1000000000000002554 ) ;
#6818=CIRCLE ( 'NONE', #10002, 6.750000000000000000 ) ;
#6819=AXIS2_PLACEMENT_3D ( 'NONE', #2339, #10048, #10856 ) ;
#6835=AXIS2_PLACEMENT_3D ( 'NONE', #11998, #4508, #2747 ) ;
#6871=DIRECTION ( 'NONE',  ( 0.000000000000000000, 0.000000000000000000, -1.000000000000000000 ) ) ;
#6894=SURFACE_STYLE_FILL_AREA ( #3080 ) ;
#6902=FACE_OUTER_BOUND ( 'NONE', #5340, .T. ) ;
#6911=CARTESIAN_POINT ( 'NONE',  ( -1.499999999999999556, 6.975000000000000533, 0.000000000000000000 ) ) ;
#6918=ORIENTED_EDGE ( 'NONE', *, *, #11050, .T. ) ;
#6923=DIRECTION ( 'NONE',  ( 0.000000000000000000, -1.224646799147353454E-16, 1.000000000000000000 ) ) ;
#6935=DIRECTION ( 'NONE',  ( 0.000000000000000000, 0.000000000000000000, -1.000000000000000000 ) ) ;
#6941=DIRECTION ( 'NONE',  ( 1.000000000000000000, 0.000000000000000000, 0.000000000000000000 ) ) ;
#6950=LINE ( 'NONE', #3268, #5414 ) ;
#6951=DIRECTION ( 'NONE',  ( 1.000000000000000000, 0.000000000000000000, 0.000000000000000000 ) ) ;
#6965=CARTESIAN_POINT ( 'NONE',  ( 1.500000000000000444, 5.100000000000000533, 0.000000000000000000 ) ) ;
#6967=CIRCLE ( 'NONE', #167, 5.525000000000000355 ) ;
#6996=FACE_OUTER_BOUND ( 'NONE', #9538, .T. ) ;
#7010=DIRECTION ( 'NONE',  ( 0.000000000000000000, 0.000000000000000000, -1.000000000000000000 ) ) ;
#7012=DIRECTION ( 'NONE',  ( 1.000000000000000000, 0.000000000000000000, 0.000000000000000000 ) ) ;
#7029=AXIS2_PLACEMENT_3D ( 'NONE', #4763, #140, #3901 ) ;
#7036=DIRECTION ( 'NONE',  ( 0.000000000000000000, 0.000000000000000000, -1.000000000000000000 ) ) ;
#7044=VERTEX_POINT ( 'NONE', #5686 ) ;
#7046=AXIS2_PLACEMENT_3D ( 'NONE', #6965, #4142, #7036 ) ;
#7066=ORIENTED_EDGE ( 'NONE', *, *, #366, .T. ) ;
#7072=CARTESIAN_POINT ( 'NONE',  ( -1.500000000000001332, 0.000000000000000000, 0.000000000000000000 ) ) ;
#7098=FACE_BOUND ( 'NONE', #373, .T. ) ;
#7103=ORIENTED_EDGE ( 'NONE', *, *, #4320, .T. ) ;
#7137=VERTEX_POINT ( 'NONE', #8886 ) ;
#7139=EDGE_CURVE ( 'NONE', #9876, #8263, #6967, .T. ) ;
#7166=AXIS2_PLACEMENT_3D ( 'NONE', #5175, #5940, #2300 ) ;
#7196=CARTESIAN_POINT ( 'NONE',  ( -1.400000000000000133, 0.000000000000000000, 0.000000000000000000 ) ) ;
#7201=ORIENTED_EDGE ( 'NONE', *, *, #128, .T. ) ;
#7209=CARTESIAN_POINT ( 'NONE',  ( -1.399999999999998579, 9.184850993605147944E-16, 7.500000000000000000 ) ) ;
#7228=EDGE_LOOP ( 'NONE', ( #10505, #6770, #11101, #6272 ) ) ;
#7244=CYLINDRICAL_SURFACE ( 'NONE', #4843, 7.500000000000000000 ) ;
#7245=ORIENTED_EDGE ( 'NONE', *, *, #408, .F. ) ;
#7265=ORIENTED_EDGE ( 'NONE', *, *, #9916, .F. ) ;
#7307=ADVANCED_FACE ( 'NONE', ( #2598 ), #6560, .T. ) ;
#7353=LINE ( 'NONE', #5532, #4815 ) ;
#7367=EDGE_CURVE ( 'NONE', #8107, #10292, #377, .T. ) ;
#7385=VERTEX_POINT ( 'NONE', #8429 ) ;
#7393=DIRECTION ( 'NONE',  ( 0.000000000000000000, 0.000000000000000000, -1.000000000000000000 ) ) ;
#7394=AXIS2_PLACEMENT_3D ( 'NONE', #3443, #5071, #3198 ) ;
#7401=DIRECTION ( 'NONE',  ( 0.000000000000000000, 0.000000000000000000, -1.000000000000000000 ) ) ;
#7403=ORIENTED_EDGE ( 'NONE', *, *, #5949, .T. ) ;
#7456=AXIS2_PLACEMENT_3D ( 'NONE', #500, #4186, #11743 ) ;
#7467=CARTESIAN_POINT ( 'NONE',  ( 1.500000000000001332, 0.000000000000000000, -5.525000000000000355 ) ) ;
#7468=FACE_OUTER_BOUND ( 'NONE', #5056, .T. ) ;
#7472=EDGE_LOOP ( 'NONE', ( #4257, #8916 ) ) ;
#7482=DIRECTION ( 'NONE',  ( 1.000000000000000000, 0.000000000000000000, 0.000000000000000000 ) ) ;
#7483=ORIENTED_EDGE ( 'NONE', *, *, #1964, .T. ) ;
#7500=DIRECTION ( 'NONE',  ( 0.000000000000000000, 0.000000000000000000, -1.000000000000000000 ) ) ;
#7509=DIRECTION ( 'NONE',  ( 0.000000000000000000, 0.000000000000000000, -1.000000000000000000 ) ) ;
#7540=CARTESIAN_POINT ( 'NONE',  ( 1.500000000000001332, 0.000000000000000000, 0.000000000000000000 ) ) ;
#7589=CARTESIAN_POINT ( 'NONE',  ( -1.500000000000001332, 7.041719095097280880E-16, 5.750000000000000000 ) ) ;
#7643=CARTESIAN_POINT ( 'NONE',  ( -1.500000000000001332, 9.123618653647779187E-16, 7.399999999999999467 ) ) ;
#7657=CIRCLE ( 'NONE', #5174, 0.7499999999999997780 ) ;
#7658=CYLINDRICAL_SURFACE ( 'NONE', #8653, 5.525000000000000355 ) ;
#7666=ORIENTED_EDGE ( 'NONE', *, *, #7829, .T. ) ;
#7713=FACE_OUTER_BOUND ( 'NONE', #1355, .T. ) ;
#7727=EDGE_CURVE ( 'NONE', #4119, #718, #3590, .T. ) ;
#7788=ORIENTED_EDGE ( 'NONE', *, *, #10152, .F. ) ;
#7806=VECTOR ( 'NONE', #2351, 1000.000000000000000 ) ;
#7821=VECTOR ( 'NONE', #8109, 1000.000000000000000 ) ;
#7829=EDGE_CURVE ( 'NONE', #6360, #11478, #8026, .T. ) ;
#7833=AXIS2_PLACEMENT_3D ( 'NONE', #7196, #1867, #5606 ) ;
#7895=ORIENTED_EDGE ( 'NONE', *, *, #6609, .F. ) ;
#7921=EDGE_LOOP ( 'NONE', ( #5036, #6312, #7245, #12097 ) ) ;
#7996=CARTESIAN_POINT ( 'NONE',  ( -20.63749999999999929, 6.766173565289127388E-16, 5.525000000000000355 ) ) ;
#8002=DIRECTION ( 'NONE',  ( 0.000000000000000000, 0.000000000000000000, -1.000000000000000000 ) ) ;
#8008=CIRCLE ( 'NONE', #602, 5.750000000000000000 ) ;
#8012=CIRCLE ( 'NONE', #15, 0.1000000000000002554 ) ;
#8026=LINE ( 'NONE', #2264, #11758 ) ;
#8029=EDGE_CURVE ( 'NONE', #6360, #5264, #2793, .T. ) ;
#8062=ORIENTED_EDGE ( 'NONE', *, *, #11948, .T. ) ;
#8070=CARTESIAN_POINT ( 'NONE',  ( 1.400000000000000133, 0.000000000000000000, 0.000000000000000000 ) ) ;
#8072=EDGE_CURVE ( 'NONE', #130, #7385, #5392, .T. ) ;
#8107=VERTEX_POINT ( 'NONE', #3347 ) ;
#8109=DIRECTION ( 'NONE',  ( 1.000000000000000000, 0.000000000000000000, 0.000000000000000000 ) ) ;
#8133=EDGE_LOOP ( 'NONE', ( #7103, #11156, #444, #7265 ) ) ;
#8183=ORIENTED_EDGE ( 'NONE', *, *, #135, .F. ) ;
#8203=AXIS2_PLACEMENT_3D ( 'NONE', #11726, #4235, #4350 ) ;
#8227=CIRCLE ( 'NONE', #10811, 7.399999999999999467 ) ;
#8228=DIRECTION ( 'NONE',  ( 0.000000000000000000, 0.000000000000000000, -1.000000000000000000 ) ) ;
#8243=EDGE_LOOP ( 'NONE', ( #5942, #6918, #1785, #1720 ) ) ;
#8257=AXIS2_PLACEMENT_3D ( 'NONE', #7540, #11155, #2590 ) ;
#8263=VERTEX_POINT ( 'NONE', #1773 ) ;
#8309=ORIENTED_EDGE ( 'NONE', *, *, #6476, .F. ) ;
#8333=ORIENTED_EDGE ( 'NONE', *, *, #5630, .F. ) ;
#8404=DIRECTION ( 'NONE',  ( -0.000000000000000000, 1.000000000000000000, 1.224646799147353207E-16 ) ) ;
#8416=CARTESIAN_POINT ( 'NONE',  ( -20.63749999999999929, 0.000000000000000000, 0.000000000000000000 ) ) ;
#8421=AXIS2_PLACEMENT_3D ( 'NONE', #10966, #342, #5981 ) ;
#8428=CARTESIAN_POINT ( 'NONE',  ( -1.500000000000000444, 5.750000000000000000, 0.000000000000000000 ) ) ;
#8429=CARTESIAN_POINT ( 'NONE',  ( -1.500000000000001332, 0.000000000000000000, -6.975000000000000533 ) ) ;
#8449=CARTESIAN_POINT ( 'NONE',  ( -0.5590169943749470072, 0.000000000000000000, -5.750000000000000000 ) ) ;
#8450=DIRECTION ( 'NONE',  ( -1.000000000000000000, -0.000000000000000000, -0.000000000000000000 ) ) ;
#8456=DIRECTION ( 'NONE',  ( 1.000000000000000000, 0.000000000000000000, 0.000000000000000000 ) ) ;
#8459=DIRECTION ( 'NONE',  ( 0.000000000000000000, 1.000000000000000000, -1.224646799147353207E-16 ) ) ;
#8482=FACE_OUTER_BOUND ( 'NONE', #12048, .T. ) ;
#8542=EDGE_LOOP ( 'NONE', ( #5145, #4742 ) ) ;
#8543=DIRECTION ( 'NONE',  ( 0.000000000000000000, 0.000000000000000000, -1.000000000000000000 ) ) ;
#8548=FACE_OUTER_BOUND ( 'NONE', #5722, .T. ) ;
#8558=FACE_OUTER_BOUND ( 'NONE', #5329, .T. ) ;
#8608=CIRCLE ( 'NONE', #2807, 5.000000000000000000 ) ;
#8651=CARTESIAN_POINT ( 'NONE',  ( -20.63749999999999929, 0.000000000000000000, 0.000000000000000000 ) ) ;
#8653=AXIS2_PLACEMENT_3D ( 'NONE', #8651, #2828, #8710 ) ;
#8688=EDGE_CURVE ( 'NONE', #5429, #702, #8608, .T. ) ;
#8689=ORIENTED_EDGE ( 'NONE', *, *, #87, .F. ) ;
#8710=DIRECTION ( 'NONE',  ( 0.000000000000000000, 0.000000000000000000, -1.000000000000000000 ) ) ;
#8779=ORIENTED_EDGE ( 'NONE', *, *, #11106, .F. ) ;
#8818=CARTESIAN_POINT ( 'NONE',  ( -20.63749999999999574, 0.000000000000000000, -6.750000000000000000 ) ) ;
#8848=EDGE_CURVE ( 'NONE', #1870, #10292, #6950, .T. ) ;
#8860=AXIS2_PLACEMENT_3D ( 'NONE', #11437, #9642, #7509 ) ;
#8864=DIRECTION ( 'NONE',  ( 1.000000000000000000, 0.000000000000000000, 0.000000000000000000 ) ) ;
#8874=ORIENTED_EDGE ( 'NONE', *, *, #6476, .T. ) ;
#8886=CARTESIAN_POINT ( 'NONE',  ( 1.500000000000001332, 0.000000000000000000, -7.399999999999999467 ) ) ;
#8916=ORIENTED_EDGE ( 'NONE', *, *, #3179, .T. ) ;
#8923=DIRECTION ( 'NONE',  ( 0.000000000000000000, -1.000000000000000000, 0.000000000000000000 ) ) ;
#8941=LINE ( 'NONE', #8818, #9564 ) ;
#8946=DIRECTION ( 'NONE',  ( 1.000000000000000000, 0.000000000000000000, 0.000000000000000000 ) ) ;
#8961=ORIENTED_EDGE ( 'NONE', *, *, #4110, .F. ) ;
#8968=CARTESIAN_POINT ( 'NONE',  ( -1.500000000000000888, 0.000000000000000000, -5.100000000000000533 ) ) ;
#8996=ADVANCED_FACE ( 'NONE', ( #3736 ), #5427, .T. ) ;
#9000=CARTESIAN_POINT ( 'NONE',  ( -1.500000000000001332, 0.000000000000000000, -7.399999999999999467 ) ) ;
#9002=ORIENTED_EDGE ( 'NONE', *, *, #192, .T. ) ;
#9013=TOROIDAL_SURFACE ( 'NONE', #11587, 6.250000000000000000, 0.7500000000000000000 ) ;
#9035=CIRCLE ( 'NONE', #6835, 5.525000000000000355 ) ;
#9040=( GEOMETRIC_REPRESENTATION_CONTEXT ( 3 ) GLOBAL_UNCERTAINTY_ASSIGNED_CONTEXT ( ( #9663 ) ) GLOBAL_UNIT_ASSIGNED_CONTEXT ( ( #10122, #5366, #543 ) ) REPRESENTATION_CONTEXT ( 'NONE', 'WORKASPACE' ) );
#9044=CIRCLE ( 'NONE', #6044, 7.500000000000000000 ) ;
#9069=DIRECTION ( 'NONE',  ( 1.000000000000000000, 0.000000000000000000, 0.000000000000000000 ) ) ;
#9070=DIRECTION ( 'NONE',  ( 1.000000000000000000, 0.000000000000000000, 0.000000000000000000 ) ) ;
#9073=STYLED_ITEM('',(#12398),#4380);
#9108=AXIS2_PLACEMENT_3D ( 'NONE', #865, #56, #927 ) ;
#9123=DIRECTION ( 'NONE',  ( 0.000000000000000000, 0.000000000000000000, -1.000000000000000000 ) ) ;
#9172=ORIENTED_EDGE ( 'NONE', *, *, #10349, .F. ) ;
#9206=TOROIDAL_SURFACE ( 'NONE', #3812, 7.399999999999999467, 0.1000000000000000472 ) ;
#9298=CIRCLE ( 'NONE', #489, 6.975000000000000533 ) ;
#9325=LINE ( 'NONE', #6320, #12022 ) ;
#9326=CARTESIAN_POINT ( 'NONE',  ( -0.1920286436967154065, 0.000000000000000000, 6.975000000000000533 ) ) ;
#9342=CYLINDRICAL_SURFACE ( 'NONE', #5428, 6.975000000000000533 ) ;
#9346=DIRECTION ( 'NONE',  ( -1.000000000000000000, -0.000000000000000000, -0.000000000000000000 ) ) ;
#9355=EDGE_CURVE ( 'NONE', #5401, #9980, #3049, .T. ) ;
#9363=CARTESIAN_POINT ( 'NONE',  ( 1.399999999999999689, 0.000000000000000000, 0.000000000000000000 ) ) ;
#9389=AXIS2_PLACEMENT_3D ( 'NONE', #3825, #12249, #11498 ) ;
#9402=DIRECTION ( 'NONE',  ( 0.000000000000000000, -1.224646799147353454E-16, 1.000000000000000000 ) ) ;
#9411=DIRECTION ( 'NONE',  ( -1.000000000000000000, -0.000000000000000000, -0.000000000000000000 ) ) ;
#9453=CARTESIAN_POINT ( 'NONE',  ( 0.000000000000000000, 0.000000000000000000, 0.000000000000000000 ) ) ;
#9457=DIRECTION ( 'NONE',  ( 1.000000000000000000, 0.000000000000000000, 0.000000000000000000 ) ) ;
#9460=FACE_OUTER_BOUND ( 'NONE', #6451, .T. ) ;
#9471=ORIENTED_EDGE ( 'NONE', *, *, #135, .T. ) ;
#9477=CIRCLE ( 'NONE', #5276, 6.975000000000000533 ) ;
#9527=UNCERTAINTY_MEASURE_WITH_UNIT (LENGTH_MEASURE( 1.000000000000000082E-05 ), #1597, 'distance_accuracy_value', 'NONE');
#9530=EDGE_CURVE ( 'NONE', #5710, #702, #2233, .T. ) ;
#9538=EDGE_LOOP ( 'NONE', ( #9002, #5304, #7201, #12218 ) ) ;
#9564=VECTOR ( 'NONE', #6941, 1000.000000000000000 ) ;
#9566=FACE_OUTER_BOUND ( 'NONE', #3928, .T. ) ;
#9574=TOROIDAL_SURFACE ( 'NONE', #11354, 6.250000000000000000, 0.7500000000000000000 ) ;
#9592=CIRCLE ( 'NONE', #613, 6.750000000000000000 ) ;
#9642=DIRECTION ( 'NONE',  ( 1.000000000000000000, 0.000000000000000000, 0.000000000000000000 ) ) ;
#9646=CYLINDRICAL_SURFACE ( 'NONE', #11272, 5.000000000000000000 ) ;
#9653=DIRECTION ( 'NONE',  ( 1.000000000000000000, 0.000000000000000000, 0.000000000000000000 ) ) ;
#9658=DIRECTION ( 'NONE',  ( 1.000000000000000000, 0.000000000000000000, 0.000000000000000000 ) ) ;
#9663=UNCERTAINTY_MEASURE_WITH_UNIT (LENGTH_MEASURE( 1.000000000000000082E-05 ), #10122, 'distance_accuracy_value', 'NONE');
#9682=ADVANCED_FACE ( 'NONE', ( #9909, #7098 ), #9961, .T. ) ;
#9699=CARTESIAN_POINT ( 'NONE',  ( 1.400000000000001910, 6.184466335694134054E-16, 5.000000000000000000 ) ) ;
#9723=ORIENTED_EDGE ( 'NONE', *, *, #7139, .F. ) ;
#9756=DIRECTION ( 'NONE',  ( 0.000000000000000000, -1.000000000000000000, 0.000000000000000000 ) ) ;
#9766=TOROIDAL_SURFACE ( 'NONE', #4570, 5.100000000000000533, 0.1000000000000001582 ) ;
#9775=AXIS2_PLACEMENT_3D ( 'NONE', #8070, #11967, #10978 ) ;
#9784=ADVANCED_FACE ( 'NONE', ( #5089 ), #328, .T. ) ;
#9805=CIRCLE ( 'NONE', #8203, 6.750000000000000000 ) ;
#9816=ORIENTED_EDGE ( 'NONE', *, *, #11274, .T. ) ;
#9830=COLOUR_RGB ( '',1.000000000000000000, 0.9490196078431372140, 0.9098039215686274384 ) ;
#9839=CARTESIAN_POINT ( 'NONE',  ( 1.500000000000001332, 0.000000000000000000, 0.000000000000000000 ) ) ;
#9876=VERTEX_POINT ( 'NONE', #7467 ) ;
#9887=DIRECTION ( 'NONE',  ( 1.000000000000000000, 0.000000000000000000, 0.000000000000000000 ) ) ;
#9891=CIRCLE ( 'NONE', #12263, 5.750000000000000000 ) ;
#9909=FACE_OUTER_BOUND ( 'NONE', #3856, .T. ) ;
#9916=EDGE_CURVE ( 'NONE', #5423, #5429, #3252, .T. ) ;
#9954=ORIENTED_EDGE ( 'NONE', *, *, #7367, .T. ) ;
#9957=EDGE_CURVE ( 'NONE', #9980, #5401, #51, .T. ) ;
#9961=PLANE ( 'NONE',  #7046 ) ;
#9970=AXIS2_PLACEMENT_3D ( 'NONE', #11422, #5736, #7500 ) ;
#9976=ADVANCED_FACE ( 'NONE', ( #6902 ), #7658, .T. ) ;
#9980=VERTEX_POINT ( 'NONE', #1896 ) ;
#9994=PRODUCT_DEFINITION ( 'UNKNOWN', '', #1858, #6140 ) ;
#9997=ORIENTED_EDGE ( 'NONE', *, *, #9530, .F. ) ;
#10002=AXIS2_PLACEMENT_3D ( 'NONE', #9839, #6951, #10702 ) ;
#10016=ORIENTED_EDGE ( 'NONE', *, *, #9957, .T. ) ;
#10039=CARTESIAN_POINT ( 'NONE',  ( -20.63749999999999929, 7.041719095097280880E-16, 5.750000000000000000 ) ) ;
#10048=DIRECTION ( 'NONE',  ( 1.000000000000000000, 0.000000000000000000, 0.000000000000000000 ) ) ;
#10060=CARTESIAN_POINT ( 'NONE',  ( -0.5590169943749470072, 0.000000000000000000, 0.000000000000000000 ) ) ;
#10078=DIRECTION ( 'NONE',  ( 1.000000000000000000, 0.000000000000000000, 0.000000000000000000 ) ) ;
#10102=LINE ( 'NONE', #3531, #781 ) ;
#10122=( LENGTH_UNIT ( ) NAMED_UNIT ( * ) SI_UNIT ( .MILLI., .METRE. ) );
#10147=CARTESIAN_POINT ( 'NONE',  ( -20.63749999999999574, 0.000000000000000000, 0.000000000000000000 ) ) ;
#10152=EDGE_CURVE ( 'NONE', #11478, #720, #10435, .T. ) ;
#10153=CARTESIAN_POINT ( 'NONE',  ( -0.5590169943749470072, 0.000000000000000000, 0.000000000000000000 ) ) ;
#10217=EDGE_CURVE ( 'NONE', #1460, #5429, #9325, .T. ) ;
#10237=DIRECTION ( 'NONE',  ( 1.000000000000000000, 0.000000000000000000, 0.000000000000000000 ) ) ;
#10239=VERTEX_POINT ( 'NONE', #10307 ) ;
#10244=DIRECTION ( 'NONE',  ( 0.000000000000000000, 1.000000000000000000, -1.224646799147353207E-16 ) ) ;
#10259=CIRCLE ( 'NONE', #5086, 6.750000000000000000 ) ;
#10261=CARTESIAN_POINT ( 'NONE',  ( -1.500000000000001332, 0.000000000000000000, -5.750000000000000000 ) ) ;
#10273=ORIENTED_EDGE ( 'NONE', *, *, #4888, .F. ) ;
#10292=VERTEX_POINT ( 'NONE', #8449 ) ;
#10307=CARTESIAN_POINT ( 'NONE',  ( 0.5590169943749478954, 0.000000000000000000, 6.750000000000000000 ) ) ;
#10311=CARTESIAN_POINT ( 'NONE',  ( -20.63749999999999929, 6.123233995736766282E-16, 5.000000000000000000 ) ) ;
#10320=DIRECTION ( 'NONE',  ( 0.000000000000000000, -1.000000000000000000, 0.000000000000000000 ) ) ;
#10321=DIRECTION ( 'NONE',  ( 1.000000000000000000, 0.000000000000000000, 0.000000000000000000 ) ) ;
#10324=FACE_OUTER_BOUND ( 'NONE', #4708, .T. ) ;
#10337=ORIENTED_EDGE ( 'NONE', *, *, #11603, .T. ) ;
#10339=SHAPE_DEFINITION_REPRESENTATION ( #11609, #11292 ) ;
#10342=ADVANCED_FACE ( 'NONE', ( #1745 ), #9766, .T. ) ;
#10349=EDGE_CURVE ( 'NONE', #7385, #3952, #10632, .T. ) ;
#10369=DIRECTION ( 'NONE',  ( 0.000000000000000000, 0.000000000000000000, 1.000000000000000000 ) ) ;
#10371=ORIENTED_EDGE ( 'NONE', *, *, #4149, .F. ) ;
#10387=CARTESIAN_POINT ( 'NONE',  ( 1.499999999999999778, 7.399999999999999467, 0.000000000000000000 ) ) ;
#10435=CIRCLE ( 'NONE', #7456, 7.500000000000000000 ) ;
#10448=ADVANCED_FACE ( 'NONE', ( #12298 ), #2805, .F. ) ;
#10452=CARTESIAN_POINT ( 'NONE',  ( -20.63749999999999929, 0.000000000000000000, 0.000000000000000000 ) ) ;
#10490=CIRCLE ( 'NONE', #9108, 5.000000000000000000 ) ;
#10505=ORIENTED_EDGE ( 'NONE', *, *, #366, .F. ) ;
#10562=ADVANCED_FACE ( 'NONE', ( #6996 ), #3768, .T. ) ;
#10568=DIRECTION ( 'NONE',  ( 0.000000000000000000, 0.000000000000000000, -1.000000000000000000 ) ) ;
#10612=ORIENTED_EDGE ( 'NONE', *, *, #12280, .T. ) ;
#10614=EDGE_CURVE ( 'NONE', #7044, #5044, #8941, .T. ) ;
#10632=LINE ( 'NONE', #2880, #1980 ) ;
#10695=SURFACE_SIDE_STYLE ('',( #6894 ) ) ;
#10697=CARTESIAN_POINT ( 'NONE',  ( 1.500000000000000888, 0.000000000000000000, -5.100000000000000533 ) ) ;
#10702=DIRECTION ( 'NONE',  ( 0.000000000000000000, 0.000000000000000000, -1.000000000000000000 ) ) ;
#10705=ORIENTED_EDGE ( 'NONE', *, *, #2650, .F. ) ;
#10706=DIRECTION ( 'NONE',  ( 1.000000000000000000, 0.000000000000000000, 0.000000000000000000 ) ) ;
#10726=DIRECTION ( 'NONE',  ( 1.000000000000000000, 0.000000000000000000, 0.000000000000000000 ) ) ;
#10751=ADVANCED_FACE ( 'NONE', ( #12098 ), #9574, .T. ) ;
#10780=CIRCLE ( 'NONE', #6592, 5.100000000000000533 ) ;
#10798=DIRECTION ( 'NONE',  ( 1.000000000000000000, 0.000000000000000000, 0.000000000000000000 ) ) ;
#10807=DIRECTION ( 'NONE',  ( 1.000000000000000000, 0.000000000000000000, 0.000000000000000000 ) ) ;
#10811=AXIS2_PLACEMENT_3D ( 'NONE', #11852, #9069, #9123 ) ;
#10830=EDGE_LOOP ( 'NONE', ( #10612, #6520 ) ) ;
#10856=DIRECTION ( 'NONE',  ( 0.000000000000000000, 0.000000000000000000, -1.000000000000000000 ) ) ;
#10873=( NAMED_UNIT ( * ) PLANE_ANGLE_UNIT ( ) SI_UNIT ( $, .RADIAN. ) );
#10892=DIRECTION ( 'NONE',  ( -0.000000000000000000, 0.000000000000000000, 1.000000000000000000 ) ) ;
#10899=DIRECTION ( 'NONE',  ( 0.000000000000000000, -1.000000000000000000, 0.000000000000000000 ) ) ;
#10904=CARTESIAN_POINT ( 'NONE',  ( 0.000000000000000000, 7.654042494670957606E-16, -6.250000000000000000 ) ) ;
#10906=FACE_OUTER_BOUND ( 'NONE', #7921, .T. ) ;
#10912=ADVANCED_FACE ( 'NONE', ( #8558 ), #4613, .T. ) ;
#10926=ORIENTED_EDGE ( 'NONE', *, *, #8072, .F. ) ;
#10966=CARTESIAN_POINT ( 'NONE',  ( -20.63749999999999574, 0.000000000000000000, 0.000000000000000000 ) ) ;
#10978=DIRECTION ( 'NONE',  ( 0.000000000000000000, 0.000000000000000000, -1.000000000000000000 ) ) ;
#11021=AXIS2_PLACEMENT_3D ( 'NONE', #6521, #10320, #1759 ) ;
#11042=CARTESIAN_POINT ( 'NONE',  ( -20.63749999999999574, 0.000000000000000000, 0.000000000000000000 ) ) ;
#11048=EDGE_CURVE ( 'NONE', #3603, #8107, #814, .T. ) ;
#11050=EDGE_CURVE ( 'NONE', #10239, #4391, #464, .T. ) ;
#11055=( GEOMETRIC_REPRESENTATION_CONTEXT ( 3 ) GLOBAL_UNCERTAINTY_ASSIGNED_CONTEXT ( ( #9527 ) ) GLOBAL_UNIT_ASSIGNED_CONTEXT ( ( #1597, #4411, #12036 ) ) REPRESENTATION_CONTEXT ( 'NONE', 'WORKASPACE' ) );
#11075=DIRECTION ( 'NONE',  ( -1.000000000000000000, -0.000000000000000000, -0.000000000000000000 ) ) ;
#11086=AXIS2_PLACEMENT_3D ( 'NONE', #6440, #10244, #5501 ) ;
#11090=ORIENTED_EDGE ( 'NONE', *, *, #10217, .T. ) ;
#11091=CARTESIAN_POINT ( 'NONE',  ( -0.1920286436967153787, 0.000000000000000000, 0.000000000000000000 ) ) ;
#11094=DIRECTION ( 'NONE',  ( 0.000000000000000000, 0.000000000000000000, 1.000000000000000000 ) ) ;
#11101=ORIENTED_EDGE ( 'NONE', *, *, #1190, .T. ) ;
#11106=EDGE_CURVE ( 'NONE', #4934, #8107, #3343, .T. ) ;
#11142=ORIENTED_EDGE ( 'NONE', *, *, #1783, .T. ) ;
#11155=DIRECTION ( 'NONE',  ( 1.000000000000000000, 0.000000000000000000, 0.000000000000000000 ) ) ;
#11156=ORIENTED_EDGE ( 'NONE', *, *, #9530, .T. ) ;
#11187=ORIENTED_EDGE ( 'NONE', *, *, #2712, .F. ) ;
#11196=TOROIDAL_SURFACE ( 'NONE', #5823, 7.399999999999999467, 0.1000000000000000472 ) ;
#11220=ORIENTED_EDGE ( 'NONE', *, *, #9355, .T. ) ;
#11251=EDGE_CURVE ( 'NONE', #3952, #10292, #2609, .T. ) ;
#11256=ADVANCED_FACE ( 'NONE', ( #10324 ), #9342, .F. ) ;
#11264=CYLINDRICAL_SURFACE ( 'NONE', #6243, 7.500000000000000000 ) ;
#11272=AXIS2_PLACEMENT_3D ( 'NONE', #11496, #8456, #12246 ) ;
#11274=EDGE_CURVE ( 'NONE', #5710, #5423, #4208, .T. ) ;
#11292=SHAPE_REPRESENTATION ( 'angular contact ball bearing_68_iso_ISO 15 ABB - 1710 - 20,SI,NC,20_68', ( #6056 ), #6426 ) ;
#11298=ORIENTED_EDGE ( 'NONE', *, *, #7829, .F. ) ;
#11301=EDGE_LOOP ( 'NONE', ( #10705, #4964, #2099, #1141 ) ) ;
#11343=CARTESIAN_POINT ( 'NONE',  ( 0.000000000000000000, 0.000000000000000000, 0.000000000000000000 ) ) ;
#11354=AXIS2_PLACEMENT_3D ( 'NONE', #6435, #1736, #2677 ) ;
#11378=DIRECTION ( 'NONE',  ( 0.000000000000000000, 0.000000000000000000, -1.000000000000000000 ) ) ;
#11386=ORIENTED_EDGE ( 'NONE', *, *, #10217, .F. ) ;
#11416=EDGE_LOOP ( 'NONE', ( #2882, #1865 ) ) ;
#11422=CARTESIAN_POINT ( 'NONE',  ( -20.63749999999999929, 0.000000000000000000, 0.000000000000000000 ) ) ;
#11437=CARTESIAN_POINT ( 'NONE',  ( -20.63749999999999574, 0.000000000000000000, 0.000000000000000000 ) ) ;
#11442=AXIS2_PLACEMENT_3D ( 'NONE', #12176, #1886, #935 ) ;
#11478=VERTEX_POINT ( 'NONE', #3279 ) ;
#11480=VERTEX_POINT ( 'NONE', #11695 ) ;
#11490=DIRECTION ( 'NONE',  ( 0.000000000000000000, 0.000000000000000000, -1.000000000000000000 ) ) ;
#11496=CARTESIAN_POINT ( 'NONE',  ( -20.63749999999999929, 0.000000000000000000, 0.000000000000000000 ) ) ;
#11498=DIRECTION ( 'NONE',  ( 0.000000000000000000, 0.000000000000000000, -1.000000000000000000 ) ) ;
#11559=FACE_OUTER_BOUND ( 'NONE', #10830, .T. ) ;
#11587=AXIS2_PLACEMENT_3D ( 'NONE', #11343, #2864, #4793 ) ;
#11603=EDGE_CURVE ( 'NONE', #8263, #9876, #9035, .T. ) ;
#11609=PRODUCT_DEFINITION_SHAPE ( 'NONE', 'NONE',  #9994 ) ;
#11622=ORIENTED_EDGE ( 'NONE', *, *, #5468, .F. ) ;
#11623=CARTESIAN_POINT ( 'NONE',  ( 1.500000000000001332, 0.000000000000000000, 0.000000000000000000 ) ) ;
#11624=FILL_AREA_STYLE_COLOUR ( '', #9830 ) ;
#11631=CIRCLE ( 'NONE', #8257, 7.399999999999999467 ) ;
#11686=CARTESIAN_POINT ( 'NONE',  ( 0.1920286436967153787, 0.000000000000000000, 5.525000000000000355 ) ) ;
#11695=CARTESIAN_POINT ( 'NONE',  ( -1.500000000000000888, 6.245698675651501825E-16, 5.100000000000000533 ) ) ;
#11726=CARTESIAN_POINT ( 'NONE',  ( 0.5590169943749477843, 0.000000000000000000, 0.000000000000000000 ) ) ;
#11743=DIRECTION ( 'NONE',  ( 0.000000000000000000, 0.000000000000000000, -1.000000000000000000 ) ) ;
#11757=AXIS2_PLACEMENT_3D ( 'NONE', #11091, #9346, #8228 ) ;
#11758=VECTOR ( 'NONE', #10706, 1000.000000000000000 ) ;
#11781=TOROIDAL_SURFACE ( 'NONE', #796, 7.399999999999999467, 0.1000000000000000472 ) ;
#11798=AXIS2_PLACEMENT_3D ( 'NONE', #2646, #8404, #9402 ) ;
#11807=DIRECTION ( 'NONE',  ( 0.000000000000000000, 1.224646799147353207E-16, 1.000000000000000000 ) ) ;
#11837=DIRECTION ( 'NONE',  ( 0.000000000000000000, 0.000000000000000000, -1.000000000000000000 ) ) ;
#11852=CARTESIAN_POINT ( 'NONE',  ( -1.500000000000001332, 0.000000000000000000, 0.000000000000000000 ) ) ;
#11901=FACE_OUTER_BOUND ( 'NONE', #2874, .T. ) ;
#11948=EDGE_CURVE ( 'NONE', #720, #11478, #9044, .T. ) ;
#11952=AXIS2_PLACEMENT_3D ( 'NONE', #4640, #8459, #11807 ) ;
#11967=DIRECTION ( 'NONE',  ( 1.000000000000000000, 0.000000000000000000, 0.000000000000000000 ) ) ;
#11971=CIRCLE ( 'NONE', #6641, 5.000000000000000000 ) ;
#11987=AXIS2_PLACEMENT_3D ( 'NONE', #2393, #10899, #11837 ) ;
#11998=CARTESIAN_POINT ( 'NONE',  ( 1.500000000000001332, 0.000000000000000000, 0.000000000000000000 ) ) ;
#12022=VECTOR ( 'NONE', #798, 1000.000000000000000 ) ;
#12036=( NAMED_UNIT ( * ) SI_UNIT ( $, .STERADIAN. ) SOLID_ANGLE_UNIT ( ) );
#12045=ADVANCED_FACE ( 'NONE', ( #11901 ), #7244, .T. ) ;
#12048=EDGE_LOOP ( 'NONE', ( #7483, #4504, #286, #3709 ) ) ;
#12084=DIRECTION ( 'NONE',  ( 1.000000000000000000, 0.000000000000000000, 0.000000000000000000 ) ) ;
#12096=DIRECTION ( 'NONE',  ( 0.000000000000000000, 0.000000000000000000, -1.000000000000000000 ) ) ;
#12097=ORIENTED_EDGE ( 'NONE', *, *, #4302, .F. ) ;
#12098=FACE_OUTER_BOUND ( 'NONE', #4387, .T. ) ;
#12103=ADVANCED_BREP_SHAPE_REPRESENTATION ( '', ( #4380, #6056 ), #6426 ) ;
#12117=DIRECTION ( 'NONE',  ( 0.000000000000000000, 0.000000000000000000, -1.000000000000000000 ) ) ;
#12121=DIRECTION ( 'NONE',  ( 1.000000000000000000, 0.000000000000000000, 0.000000000000000000 ) ) ;
#12141=ORIENTED_EDGE ( 'NONE', *, *, #5689, .F. ) ;
#12148=FACE_BOUND ( 'NONE', #7472, .T. ) ;
#12176=CARTESIAN_POINT ( 'NONE',  ( -1.399999999999999689, 0.000000000000000000, -7.399999999999999467 ) ) ;
#12179=TOROIDAL_SURFACE ( 'NONE', #6819, 5.100000000000000533, 0.1000000000000001582 ) ;
#12216=PRODUCT_CONTEXT ( 'NONE', #18, 'mechanical' ) ;
#12218=ORIENTED_EDGE ( 'NONE', *, *, #11048, .F. ) ;
#12231=ORIENTED_EDGE ( 'NONE', *, *, #7727, .T. ) ;
#12246=DIRECTION ( 'NONE',  ( 0.000000000000000000, 0.000000000000000000, -1.000000000000000000 ) ) ;
#12249=DIRECTION ( 'NONE',  ( 1.000000000000000000, 0.000000000000000000, 0.000000000000000000 ) ) ;
#12257=ORIENTED_EDGE ( 'NONE', *, *, #749, .T. ) ;
#12263=AXIS2_PLACEMENT_3D ( 'NONE', #7072, #9887, #252 ) ;
#12280=EDGE_CURVE ( 'NONE', #7137, #710, #11631, .T. ) ;
#12298=FACE_OUTER_BOUND ( 'NONE', #8243, .T. ) ;
#12311=DIRECTION ( 'NONE',  ( 0.000000000000000000, 0.000000000000000000, -1.000000000000000000 ) ) ;
#12317=CARTESIAN_POINT ( 'NONE',  ( 0.5590169943749477843, 0.000000000000000000, 0.000000000000000000 ) ) ;
#12330=AXIS2_PLACEMENT_3D ( 'NONE', #2638, #12121, #5278 ) ;
#12336=CARTESIAN_POINT ( 'NONE',  ( -1.399999999999999689, 0.000000000000000000, 0.000000000000000000 ) ) ;
#12342=DIRECTION ( 'NONE',  ( 0.000000000000000000, 0.000000000000000000, -1.000000000000000000 ) ) ;
#12392=COLOUR_RGB('Grey',0.48,0.52,0.57);
#12393=FILL_AREA_STYLE_COLOUR('',#12392);
#12394=FILL_AREA_STYLE('',(#12393));
#12395=SURFACE_STYLE_FILL_AREA(#12394);
#12396=SURFACE_SIDE_STYLE('',(#12395));
#12397=SURFACE_STYLE_USAGE(.BOTH.,#12396);
#12398=PRESENTATION_STYLE_ASSIGNMENT((#12397));
ENDSEC;
END-ISO-10303-21;
